ISO-10303-21;
HEADER;
/* Generated by software containing ST-Developer
 * from STEP Tools, Inc. (www.steptools.com) 
 */

FILE_DESCRIPTION(
/* description */ (''),
/* implementation_level */ '2;1');

FILE_NAME(
/* name */ 'Bracket_01.step',
/* time_stamp */ '2026-10-22T16:03:28+06:00',
/* author */ (''),
/* organization */ (''),
/* preprocessor_version */ 'ST-DEVELOPER v20.2',
/* originating_system */ 'Autodesk Translation Framework v15.15.0.0',
/* authorisation */ '');

FILE_SCHEMA (('AUTOMOTIVE_DESIGN { 1 0 10303 214 3 1 1 }'));
ENDSEC;

DATA;
#10=MECHANICAL_DESIGN_GEOMETRIC_PRESENTATION_REPRESENTATION('',(#91),#6096);
#69=SHAPE_REPRESENTATION_RELATIONSHIP('SRR','None',#6144,#80);
#80=ADVANCED_BREP_SHAPE_REPRESENTATION('',(#102),#6092);
#91=STYLED_ITEM('',(#6234),#102);
#102=MANIFOLD_SOLID_BREP('Bracket_01',#3600);
#126=FACE_BOUND('',#645,.T.);
#127=FACE_BOUND('',#646,.T.);
#128=FACE_BOUND('',#647,.T.);
#129=FACE_BOUND('',#648,.T.);
#130=FACE_BOUND('',#650,.T.);
#131=FACE_BOUND('',#651,.T.);
#132=FACE_BOUND('',#652,.T.);
#133=FACE_BOUND('',#653,.T.);
#250=PLANE('',#3945);
#251=PLANE('',#3946);
#252=PLANE('',#3947);
#253=PLANE('',#3948);
#254=PLANE('',#3949);
#255=PLANE('',#3950);
#256=PLANE('',#3951);
#257=PLANE('',#3952);
#258=PLANE('',#3953);
#259=PLANE('',#3954);
#260=PLANE('',#3955);
#261=PLANE('',#3956);
#422=FACE_OUTER_BOUND('',#630,.T.);
#423=FACE_OUTER_BOUND('',#631,.T.);
#424=FACE_OUTER_BOUND('',#632,.T.);
#425=FACE_OUTER_BOUND('',#633,.T.);
#426=FACE_OUTER_BOUND('',#634,.T.);
#427=FACE_OUTER_BOUND('',#635,.T.);
#428=FACE_OUTER_BOUND('',#636,.T.);
#429=FACE_OUTER_BOUND('',#637,.T.);
#430=FACE_OUTER_BOUND('',#638,.T.);
#431=FACE_OUTER_BOUND('',#639,.T.);
#432=FACE_OUTER_BOUND('',#640,.T.);
#433=FACE_OUTER_BOUND('',#641,.T.);
#434=FACE_OUTER_BOUND('',#642,.T.);
#435=FACE_OUTER_BOUND('',#643,.T.);
#436=FACE_OUTER_BOUND('',#644,.T.);
#437=FACE_OUTER_BOUND('',#649,.T.);
#630=EDGE_LOOP('',(#3028,#3029,#3030,#3031));
#631=EDGE_LOOP('',(#3032,#3033,#3034,#3035));
#632=EDGE_LOOP('',(#3036,#3037,#3038,#3039));
#633=EDGE_LOOP('',(#3040,#3041,#3042,#3043));
#634=EDGE_LOOP('',(#3044,#3045,#3046,#3047));
#635=EDGE_LOOP('',(#3048,#3049,#3050,#3051));
#636=EDGE_LOOP('',(#3052,#3053,#3054,#3055));
#637=EDGE_LOOP('',(#3056,#3057,#3058,#3059));
#638=EDGE_LOOP('',(#3060,#3061,#3062,#3063));
#639=EDGE_LOOP('',(#3064,#3065,#3066,#3067));
#640=EDGE_LOOP('',(#3068,#3069,#3070,#3071));
#641=EDGE_LOOP('',(#3072,#3073,#3074,#3075));
#642=EDGE_LOOP('',(#3076,#3077,#3078,#3079));
#643=EDGE_LOOP('',(#3080,#3081,#3082,#3083));
#644=EDGE_LOOP('',(#3084,#3085,#3086,#3087,#3088,#3089,#3090,#3091,#3092,
#3093));
#645=EDGE_LOOP('',(#3094));
#646=EDGE_LOOP('',(#3095));
#647=EDGE_LOOP('',(#3096));
#648=EDGE_LOOP('',(#3097));
#649=EDGE_LOOP('',(#3098,#3099,#3100,#3101,#3102,#3103,#3104,#3105,#3106,
#3107));
#650=EDGE_LOOP('',(#3108));
#651=EDGE_LOOP('',(#3109));
#652=EDGE_LOOP('',(#3110));
#653=EDGE_LOOP('',(#3111));
#969=LINE('',#5717,#1348);
#970=LINE('',#5723,#1349);
#971=LINE('',#5729,#1350);
#972=LINE('',#5735,#1351);
#973=LINE('',#5740,#1352);
#974=LINE('',#5742,#1353);
#975=LINE('',#5744,#1354);
#976=LINE('',#5745,#1355);
#977=LINE('',#5748,#1356);
#978=LINE('',#5750,#1357);
#979=LINE('',#5751,#1358);
#980=LINE('',#5754,#1359);
#981=LINE('',#5756,#1360);
#982=LINE('',#5757,#1361);
#983=LINE('',#5760,#1362);
#984=LINE('',#5762,#1363);
#985=LINE('',#5763,#1364);
#986=LINE('',#5766,#1365);
#987=LINE('',#5768,#1366);
#988=LINE('',#5769,#1367);
#989=LINE('',#5772,#1368);
#990=LINE('',#5774,#1369);
#991=LINE('',#5775,#1370);
#992=LINE('',#5778,#1371);
#993=LINE('',#5780,#1372);
#994=LINE('',#5781,#1373);
#995=LINE('',#5784,#1374);
#996=LINE('',#5786,#1375);
#997=LINE('',#5787,#1376);
#998=LINE('',#5790,#1377);
#999=LINE('',#5792,#1378);
#1000=LINE('',#5793,#1379);
#1001=LINE('',#5795,#1380);
#1002=LINE('',#5796,#1381);
#1348=VECTOR('',#4704,1.99999999999999);
#1349=VECTOR('',#4711,1.99999999999999);
#1350=VECTOR('',#4718,1.99999999999999);
#1351=VECTOR('',#4725,1.99999999999999);
#1352=VECTOR('',#4730,10.);
#1353=VECTOR('',#4731,10.);
#1354=VECTOR('',#4732,10.);
#1355=VECTOR('',#4733,10.);
#1356=VECTOR('',#4736,10.);
#1357=VECTOR('',#4737,10.);
#1358=VECTOR('',#4738,10.);
#1359=VECTOR('',#4741,10.);
#1360=VECTOR('',#4742,10.);
#1361=VECTOR('',#4743,10.);
#1362=VECTOR('',#4746,10.);
#1363=VECTOR('',#4747,10.);
#1364=VECTOR('',#4748,10.);
#1365=VECTOR('',#4751,10.);
#1366=VECTOR('',#4752,10.);
#1367=VECTOR('',#4753,10.);
#1368=VECTOR('',#4756,10.);
#1369=VECTOR('',#4757,10.);
#1370=VECTOR('',#4758,10.);
#1371=VECTOR('',#4761,10.);
#1372=VECTOR('',#4762,10.);
#1373=VECTOR('',#4763,10.);
#1374=VECTOR('',#4766,10.);
#1375=VECTOR('',#4767,10.);
#1376=VECTOR('',#4768,10.);
#1377=VECTOR('',#4771,10.);
#1378=VECTOR('',#4772,10.);
#1379=VECTOR('',#4773,10.);
#1380=VECTOR('',#4776,10.);
#1381=VECTOR('',#4777,10.);
#1558=CIRCLE('',#3934,1.99999999999999);
#1559=CIRCLE('',#3935,1.99999999999999);
#1560=CIRCLE('',#3937,1.99999999999999);
#1561=CIRCLE('',#3938,1.99999999999999);
#1562=CIRCLE('',#3940,1.99999999999999);
#1563=CIRCLE('',#3941,1.99999999999999);
#1564=CIRCLE('',#3943,1.99999999999999);
#1565=CIRCLE('',#3944,1.99999999999999);
#1797=VERTEX_POINT('',#5714);
#1798=VERTEX_POINT('',#5716);
#1799=VERTEX_POINT('',#5720);
#1800=VERTEX_POINT('',#5722);
#1801=VERTEX_POINT('',#5726);
#1802=VERTEX_POINT('',#5728);
#1803=VERTEX_POINT('',#5732);
#1804=VERTEX_POINT('',#5734);
#1805=VERTEX_POINT('',#5738);
#1806=VERTEX_POINT('',#5739);
#1807=VERTEX_POINT('',#5741);
#1808=VERTEX_POINT('',#5743);
#1809=VERTEX_POINT('',#5747);
#1810=VERTEX_POINT('',#5749);
#1811=VERTEX_POINT('',#5753);
#1812=VERTEX_POINT('',#5755);
#1813=VERTEX_POINT('',#5759);
#1814=VERTEX_POINT('',#5761);
#1815=VERTEX_POINT('',#5765);
#1816=VERTEX_POINT('',#5767);
#1817=VERTEX_POINT('',#5771);
#1818=VERTEX_POINT('',#5773);
#1819=VERTEX_POINT('',#5777);
#1820=VERTEX_POINT('',#5779);
#1821=VERTEX_POINT('',#5783);
#1822=VERTEX_POINT('',#5785);
#1823=VERTEX_POINT('',#5789);
#1824=VERTEX_POINT('',#5791);
#2226=EDGE_CURVE('',#1797,#1797,#1558,.T.);
#2227=EDGE_CURVE('',#1797,#1798,#969,.T.);
#2228=EDGE_CURVE('',#1798,#1798,#1559,.T.);
#2229=EDGE_CURVE('',#1799,#1799,#1560,.T.);
#2230=EDGE_CURVE('',#1799,#1800,#970,.T.);
#2231=EDGE_CURVE('',#1800,#1800,#1561,.T.);
#2232=EDGE_CURVE('',#1801,#1801,#1562,.T.);
#2233=EDGE_CURVE('',#1801,#1802,#971,.T.);
#2234=EDGE_CURVE('',#1802,#1802,#1563,.T.);
#2235=EDGE_CURVE('',#1803,#1803,#1564,.T.);
#2236=EDGE_CURVE('',#1803,#1804,#972,.T.);
#2237=EDGE_CURVE('',#1804,#1804,#1565,.T.);
#2238=EDGE_CURVE('',#1805,#1806,#973,.T.);
#2239=EDGE_CURVE('',#1806,#1807,#974,.T.);
#2240=EDGE_CURVE('',#1808,#1807,#975,.T.);
#2241=EDGE_CURVE('',#1805,#1808,#976,.T.);
#2242=EDGE_CURVE('',#1809,#1805,#977,.T.);
#2243=EDGE_CURVE('',#1810,#1808,#978,.T.);
#2244=EDGE_CURVE('',#1809,#1810,#979,.T.);
#2245=EDGE_CURVE('',#1811,#1809,#980,.T.);
#2246=EDGE_CURVE('',#1812,#1810,#981,.T.);
#2247=EDGE_CURVE('',#1811,#1812,#982,.T.);
#2248=EDGE_CURVE('',#1813,#1811,#983,.T.);
#2249=EDGE_CURVE('',#1814,#1812,#984,.T.);
#2250=EDGE_CURVE('',#1813,#1814,#985,.T.);
#2251=EDGE_CURVE('',#1815,#1813,#986,.T.);
#2252=EDGE_CURVE('',#1816,#1814,#987,.T.);
#2253=EDGE_CURVE('',#1815,#1816,#988,.T.);
#2254=EDGE_CURVE('',#1817,#1815,#989,.T.);
#2255=EDGE_CURVE('',#1818,#1816,#990,.T.);
#2256=EDGE_CURVE('',#1817,#1818,#991,.T.);
#2257=EDGE_CURVE('',#1819,#1817,#992,.T.);
#2258=EDGE_CURVE('',#1820,#1818,#993,.T.);
#2259=EDGE_CURVE('',#1819,#1820,#994,.T.);
#2260=EDGE_CURVE('',#1821,#1819,#995,.T.);
#2261=EDGE_CURVE('',#1822,#1820,#996,.T.);
#2262=EDGE_CURVE('',#1821,#1822,#997,.T.);
#2263=EDGE_CURVE('',#1823,#1821,#998,.T.);
#2264=EDGE_CURVE('',#1824,#1822,#999,.T.);
#2265=EDGE_CURVE('',#1823,#1824,#1000,.T.);
#2266=EDGE_CURVE('',#1806,#1823,#1001,.T.);
#2267=EDGE_CURVE('',#1807,#1824,#1002,.T.);
#3028=ORIENTED_EDGE('',*,*,#2226,.F.);
#3029=ORIENTED_EDGE('',*,*,#2227,.T.);
#3030=ORIENTED_EDGE('',*,*,#2228,.T.);
#3031=ORIENTED_EDGE('',*,*,#2227,.F.);
#3032=ORIENTED_EDGE('',*,*,#2229,.F.);
#3033=ORIENTED_EDGE('',*,*,#2230,.T.);
#3034=ORIENTED_EDGE('',*,*,#2231,.T.);
#3035=ORIENTED_EDGE('',*,*,#2230,.F.);
#3036=ORIENTED_EDGE('',*,*,#2232,.F.);
#3037=ORIENTED_EDGE('',*,*,#2233,.T.);
#3038=ORIENTED_EDGE('',*,*,#2234,.T.);
#3039=ORIENTED_EDGE('',*,*,#2233,.F.);
#3040=ORIENTED_EDGE('',*,*,#2235,.F.);
#3041=ORIENTED_EDGE('',*,*,#2236,.T.);
#3042=ORIENTED_EDGE('',*,*,#2237,.T.);
#3043=ORIENTED_EDGE('',*,*,#2236,.F.);
#3044=ORIENTED_EDGE('',*,*,#2238,.T.);
#3045=ORIENTED_EDGE('',*,*,#2239,.T.);
#3046=ORIENTED_EDGE('',*,*,#2240,.F.);
#3047=ORIENTED_EDGE('',*,*,#2241,.F.);
#3048=ORIENTED_EDGE('',*,*,#2242,.T.);
#3049=ORIENTED_EDGE('',*,*,#2241,.T.);
#3050=ORIENTED_EDGE('',*,*,#2243,.F.);
#3051=ORIENTED_EDGE('',*,*,#2244,.F.);
#3052=ORIENTED_EDGE('',*,*,#2245,.T.);
#3053=ORIENTED_EDGE('',*,*,#2244,.T.);
#3054=ORIENTED_EDGE('',*,*,#2246,.F.);
#3055=ORIENTED_EDGE('',*,*,#2247,.F.);
#3056=ORIENTED_EDGE('',*,*,#2248,.T.);
#3057=ORIENTED_EDGE('',*,*,#2247,.T.);
#3058=ORIENTED_EDGE('',*,*,#2249,.F.);
#3059=ORIENTED_EDGE('',*,*,#2250,.F.);
#3060=ORIENTED_EDGE('',*,*,#2251,.T.);
#3061=ORIENTED_EDGE('',*,*,#2250,.T.);
#3062=ORIENTED_EDGE('',*,*,#2252,.F.);
#3063=ORIENTED_EDGE('',*,*,#2253,.F.);
#3064=ORIENTED_EDGE('',*,*,#2254,.T.);
#3065=ORIENTED_EDGE('',*,*,#2253,.T.);
#3066=ORIENTED_EDGE('',*,*,#2255,.F.);
#3067=ORIENTED_EDGE('',*,*,#2256,.F.);
#3068=ORIENTED_EDGE('',*,*,#2257,.T.);
#3069=ORIENTED_EDGE('',*,*,#2256,.T.);
#3070=ORIENTED_EDGE('',*,*,#2258,.F.);
#3071=ORIENTED_EDGE('',*,*,#2259,.F.);
#3072=ORIENTED_EDGE('',*,*,#2260,.T.);
#3073=ORIENTED_EDGE('',*,*,#2259,.T.);
#3074=ORIENTED_EDGE('',*,*,#2261,.F.);
#3075=ORIENTED_EDGE('',*,*,#2262,.F.);
#3076=ORIENTED_EDGE('',*,*,#2263,.T.);
#3077=ORIENTED_EDGE('',*,*,#2262,.T.);
#3078=ORIENTED_EDGE('',*,*,#2264,.F.);
#3079=ORIENTED_EDGE('',*,*,#2265,.F.);
#3080=ORIENTED_EDGE('',*,*,#2266,.T.);
#3081=ORIENTED_EDGE('',*,*,#2265,.T.);
#3082=ORIENTED_EDGE('',*,*,#2267,.F.);
#3083=ORIENTED_EDGE('',*,*,#2239,.F.);
#3084=ORIENTED_EDGE('',*,*,#2267,.T.);
#3085=ORIENTED_EDGE('',*,*,#2264,.T.);
#3086=ORIENTED_EDGE('',*,*,#2261,.T.);
#3087=ORIENTED_EDGE('',*,*,#2258,.T.);
#3088=ORIENTED_EDGE('',*,*,#2255,.T.);
#3089=ORIENTED_EDGE('',*,*,#2252,.T.);
#3090=ORIENTED_EDGE('',*,*,#2249,.T.);
#3091=ORIENTED_EDGE('',*,*,#2246,.T.);
#3092=ORIENTED_EDGE('',*,*,#2243,.T.);
#3093=ORIENTED_EDGE('',*,*,#2240,.T.);
#3094=ORIENTED_EDGE('',*,*,#2235,.T.);
#3095=ORIENTED_EDGE('',*,*,#2232,.T.);
#3096=ORIENTED_EDGE('',*,*,#2229,.T.);
#3097=ORIENTED_EDGE('',*,*,#2226,.T.);
#3098=ORIENTED_EDGE('',*,*,#2266,.F.);
#3099=ORIENTED_EDGE('',*,*,#2238,.F.);
#3100=ORIENTED_EDGE('',*,*,#2242,.F.);
#3101=ORIENTED_EDGE('',*,*,#2245,.F.);
#3102=ORIENTED_EDGE('',*,*,#2248,.F.);
#3103=ORIENTED_EDGE('',*,*,#2251,.F.);
#3104=ORIENTED_EDGE('',*,*,#2254,.F.);
#3105=ORIENTED_EDGE('',*,*,#2257,.F.);
#3106=ORIENTED_EDGE('',*,*,#2260,.F.);
#3107=ORIENTED_EDGE('',*,*,#2263,.F.);
#3108=ORIENTED_EDGE('',*,*,#2237,.F.);
#3109=ORIENTED_EDGE('',*,*,#2234,.F.);
#3110=ORIENTED_EDGE('',*,*,#2231,.F.);
#3111=ORIENTED_EDGE('',*,*,#2228,.F.);
#3389=CYLINDRICAL_SURFACE('',#3933,1.99999999999999);
#3390=CYLINDRICAL_SURFACE('',#3936,1.99999999999999);
#3391=CYLINDRICAL_SURFACE('',#3939,1.99999999999999);
#3392=CYLINDRICAL_SURFACE('',#3942,1.99999999999999);
#3529=ADVANCED_FACE('',(#422),#3389,.F.);
#3530=ADVANCED_FACE('',(#423),#3390,.F.);
#3531=ADVANCED_FACE('',(#424),#3391,.F.);
#3532=ADVANCED_FACE('',(#425),#3392,.F.);
#3533=ADVANCED_FACE('',(#426),#250,.T.);
#3534=ADVANCED_FACE('',(#427),#251,.T.);
#3535=ADVANCED_FACE('',(#428),#252,.T.);
#3536=ADVANCED_FACE('',(#429),#253,.T.);
#3537=ADVANCED_FACE('',(#430),#254,.T.);
#3538=ADVANCED_FACE('',(#431),#255,.T.);
#3539=ADVANCED_FACE('',(#432),#256,.T.);
#3540=ADVANCED_FACE('',(#433),#257,.T.);
#3541=ADVANCED_FACE('',(#434),#258,.T.);
#3542=ADVANCED_FACE('',(#435),#259,.T.);
#3543=ADVANCED_FACE('',(#436,#126,#127,#128,#129),#260,.T.);
#3544=ADVANCED_FACE('',(#437,#130,#131,#132,#133),#261,.F.);
#3600=CLOSED_SHELL('',(#3529,#3530,#3531,#3532,#3533,#3534,#3535,#3536,
#3537,#3538,#3539,#3540,#3541,#3542,#3543,#3544));
#3932=AXIS2_PLACEMENT_3D('',#5712,#4698,#4699);
#3933=AXIS2_PLACEMENT_3D('',#5713,#4700,#4701);
#3934=AXIS2_PLACEMENT_3D('',#5715,#4702,#4703);
#3935=AXIS2_PLACEMENT_3D('',#5718,#4705,#4706);
#3936=AXIS2_PLACEMENT_3D('',#5719,#4707,#4708);
#3937=AXIS2_PLACEMENT_3D('',#5721,#4709,#4710);
#3938=AXIS2_PLACEMENT_3D('',#5724,#4712,#4713);
#3939=AXIS2_PLACEMENT_3D('',#5725,#4714,#4715);
#3940=AXIS2_PLACEMENT_3D('',#5727,#4716,#4717);
#3941=AXIS2_PLACEMENT_3D('',#5730,#4719,#4720);
#3942=AXIS2_PLACEMENT_3D('',#5731,#4721,#4722);
#3943=AXIS2_PLACEMENT_3D('',#5733,#4723,#4724);
#3944=AXIS2_PLACEMENT_3D('',#5736,#4726,#4727);
#3945=AXIS2_PLACEMENT_3D('',#5737,#4728,#4729);
#3946=AXIS2_PLACEMENT_3D('',#5746,#4734,#4735);
#3947=AXIS2_PLACEMENT_3D('',#5752,#4739,#4740);
#3948=AXIS2_PLACEMENT_3D('',#5758,#4744,#4745);
#3949=AXIS2_PLACEMENT_3D('',#5764,#4749,#4750);
#3950=AXIS2_PLACEMENT_3D('',#5770,#4754,#4755);
#3951=AXIS2_PLACEMENT_3D('',#5776,#4759,#4760);
#3952=AXIS2_PLACEMENT_3D('',#5782,#4764,#4765);
#3953=AXIS2_PLACEMENT_3D('',#5788,#4769,#4770);
#3954=AXIS2_PLACEMENT_3D('',#5794,#4774,#4775);
#3955=AXIS2_PLACEMENT_3D('',#5797,#4778,#4779);
#3956=AXIS2_PLACEMENT_3D('',#5798,#4780,#4781);
#4698=DIRECTION('axis',(0.,0.,1.));
#4699=DIRECTION('refdir',(1.,0.,0.));
#4700=DIRECTION('center_axis',(0.,-1.,0.));
#4701=DIRECTION('ref_axis',(1.,0.,0.));
#4702=DIRECTION('center_axis',(0.,1.,0.));
#4703=DIRECTION('ref_axis',(1.,0.,0.));
#4704=DIRECTION('',(0.,1.,0.));
#4705=DIRECTION('center_axis',(0.,1.,0.));
#4706=DIRECTION('ref_axis',(1.,0.,0.));
#4707=DIRECTION('center_axis',(0.,-1.,0.));
#4708=DIRECTION('ref_axis',(1.,0.,0.));
#4709=DIRECTION('center_axis',(0.,1.,0.));
#4710=DIRECTION('ref_axis',(1.,0.,0.));
#4711=DIRECTION('',(0.,1.,0.));
#4712=DIRECTION('center_axis',(0.,1.,0.));
#4713=DIRECTION('ref_axis',(1.,0.,0.));
#4714=DIRECTION('center_axis',(0.,-1.,0.));
#4715=DIRECTION('ref_axis',(1.,0.,0.));
#4716=DIRECTION('center_axis',(0.,1.,0.));
#4717=DIRECTION('ref_axis',(1.,0.,0.));
#4718=DIRECTION('',(0.,1.,0.));
#4719=DIRECTION('center_axis',(0.,1.,0.));
#4720=DIRECTION('ref_axis',(1.,0.,0.));
#4721=DIRECTION('center_axis',(0.,-1.,0.));
#4722=DIRECTION('ref_axis',(1.,0.,0.));
#4723=DIRECTION('center_axis',(0.,1.,0.));
#4724=DIRECTION('ref_axis',(1.,0.,0.));
#4725=DIRECTION('',(0.,1.,0.));
#4726=DIRECTION('center_axis',(0.,1.,0.));
#4727=DIRECTION('ref_axis',(1.,0.,0.));
#4728=DIRECTION('center_axis',(0.,0.,-1.));
#4729=DIRECTION('ref_axis',(1.,0.,0.));
#4730=DIRECTION('',(1.,0.,0.));
#4731=DIRECTION('',(0.,-1.,0.));
#4732=DIRECTION('',(1.,0.,0.));
#4733=DIRECTION('',(0.,-1.,0.));
#4734=DIRECTION('center_axis',(1.,0.,0.));
#4735=DIRECTION('ref_axis',(0.,0.,1.));
#4736=DIRECTION('',(0.,0.,1.));
#4737=DIRECTION('',(0.,0.,1.));
#4738=DIRECTION('',(0.,-1.,0.));
#4739=DIRECTION('center_axis',(0.,0.,1.));
#4740=DIRECTION('ref_axis',(-1.,0.,0.));
#4741=DIRECTION('',(-1.,0.,0.));
#4742=DIRECTION('',(-1.,0.,0.));
#4743=DIRECTION('',(0.,-1.,0.));
#4744=DIRECTION('center_axis',(1.,0.,0.));
#4745=DIRECTION('ref_axis',(0.,0.,1.));
#4746=DIRECTION('',(0.,0.,1.));
#4747=DIRECTION('',(0.,0.,1.));
#4748=DIRECTION('',(0.,-1.,0.));
#4749=DIRECTION('center_axis',(0.,0.,-1.));
#4750=DIRECTION('ref_axis',(1.,0.,0.));
#4751=DIRECTION('',(1.,0.,0.));
#4752=DIRECTION('',(1.,0.,0.));
#4753=DIRECTION('',(0.,-1.,0.));
#4754=DIRECTION('center_axis',(-1.,0.,0.));
#4755=DIRECTION('ref_axis',(0.,0.,-1.));
#4756=DIRECTION('',(0.,0.,-1.));
#4757=DIRECTION('',(0.,0.,-1.));
#4758=DIRECTION('',(0.,-1.,0.));
#4759=DIRECTION('center_axis',(0.,0.,1.));
#4760=DIRECTION('ref_axis',(-1.,0.,0.));
#4761=DIRECTION('',(-1.,0.,0.));
#4762=DIRECTION('',(-1.,0.,0.));
#4763=DIRECTION('',(0.,-1.,0.));
#4764=DIRECTION('center_axis',(1.,0.,0.));
#4765=DIRECTION('ref_axis',(0.,0.,1.));
#4766=DIRECTION('',(0.,0.,1.));
#4767=DIRECTION('',(0.,0.,1.));
#4768=DIRECTION('',(0.,-1.,0.));
#4769=DIRECTION('center_axis',(0.,0.,-1.));
#4770=DIRECTION('ref_axis',(1.,0.,0.));
#4771=DIRECTION('',(1.,0.,0.));
#4772=DIRECTION('',(1.,0.,0.));
#4773=DIRECTION('',(0.,-1.,0.));
#4774=DIRECTION('center_axis',(-1.,0.,0.));
#4775=DIRECTION('ref_axis',(0.,0.,-1.));
#4776=DIRECTION('',(0.,0.,-1.));
#4777=DIRECTION('',(0.,0.,-1.));
#4778=DIRECTION('center_axis',(0.,-1.,0.));
#4779=DIRECTION('ref_axis',(1.,0.,0.));
#4780=DIRECTION('center_axis',(0.,-1.,0.));
#4781=DIRECTION('ref_axis',(1.,0.,0.));
#5712=CARTESIAN_POINT('',(0.,0.,0.));
#5713=CARTESIAN_POINT('Origin',(-31.6092837386808,245.5,108.939950998448));
#5714=CARTESIAN_POINT('',(-33.6092837386808,242.5,108.939950998448));
#5715=CARTESIAN_POINT('Origin',(-31.6092837386808,242.5,108.939950998448));
#5716=CARTESIAN_POINT('',(-33.6092837386808,245.5,108.939950998448));
#5717=CARTESIAN_POINT('',(-33.6092837386808,245.5,108.939950998448));
#5718=CARTESIAN_POINT('Origin',(-31.6092837386808,245.5,108.939950998448));
#5719=CARTESIAN_POINT('Origin',(-71.0061608111161,245.5,95.0000000000015));
#5720=CARTESIAN_POINT('',(-73.0061608111161,242.5,95.0000000000015));
#5721=CARTESIAN_POINT('Origin',(-71.0061608111161,242.5,95.0000000000015));
#5722=CARTESIAN_POINT('',(-73.0061608111161,245.5,95.0000000000015));
#5723=CARTESIAN_POINT('',(-73.0061608111161,245.5,95.0000000000015));
#5724=CARTESIAN_POINT('Origin',(-71.0061608111161,245.5,95.0000000000015));
#5725=CARTESIAN_POINT('Origin',(-28.0061608111161,245.5,95.0000000000015));
#5726=CARTESIAN_POINT('',(-30.0061608111161,242.5,95.0000000000015));
#5727=CARTESIAN_POINT('Origin',(-28.0061608111161,242.5,95.0000000000015));
#5728=CARTESIAN_POINT('',(-30.0061608111161,245.5,95.0000000000015));
#5729=CARTESIAN_POINT('',(-30.0061608111161,245.5,95.0000000000015));
#5730=CARTESIAN_POINT('Origin',(-28.0061608111161,245.5,95.0000000000015));
#5731=CARTESIAN_POINT('Origin',(-67.4030378835514,245.5,108.939950998448));
#5732=CARTESIAN_POINT('',(-69.4030378835514,242.5,108.939950998448));
#5733=CARTESIAN_POINT('Origin',(-67.4030378835514,242.5,108.939950998448));
#5734=CARTESIAN_POINT('',(-69.4030378835514,245.5,108.939950998448));
#5735=CARTESIAN_POINT('',(-69.4030378835514,245.5,108.939950998448));
#5736=CARTESIAN_POINT('Origin',(-67.4030378835514,245.5,108.939950998448));
#5737=CARTESIAN_POINT('Origin',(-67.5061608111161,245.5,105.000000000001));
#5738=CARTESIAN_POINT('',(-67.5061608111161,245.5,105.000000000001));
#5739=CARTESIAN_POINT('',(-31.5061608111161,245.5,105.000000000001));
#5740=CARTESIAN_POINT('',(-67.5061608111161,245.5,105.000000000001));
#5741=CARTESIAN_POINT('',(-31.5061608111161,242.5,105.000000000001));
#5742=CARTESIAN_POINT('',(-31.5061608111161,245.5,105.000000000001));
#5743=CARTESIAN_POINT('',(-67.5061608111161,242.5,105.000000000001));
#5744=CARTESIAN_POINT('',(-67.5061608111161,242.5,105.000000000001));
#5745=CARTESIAN_POINT('',(-67.5061608111161,245.5,105.000000000001));
#5746=CARTESIAN_POINT('Origin',(-67.5061608111161,245.5,85.0000000000015));
#5747=CARTESIAN_POINT('',(-67.5061608111161,245.5,85.0000000000015));
#5748=CARTESIAN_POINT('',(-67.5061608111161,245.5,85.0000000000015));
#5749=CARTESIAN_POINT('',(-67.5061608111161,242.5,85.0000000000015));
#5750=CARTESIAN_POINT('',(-67.5061608111161,242.5,85.0000000000015));
#5751=CARTESIAN_POINT('',(-67.5061608111161,245.5,85.0000000000015));
#5752=CARTESIAN_POINT('Origin',(-51.5061608111161,245.5,85.0000000000015));
#5753=CARTESIAN_POINT('',(-51.5061608111161,245.5,85.0000000000015));
#5754=CARTESIAN_POINT('',(-31.5061608111161,245.5,85.0000000000015));
#5755=CARTESIAN_POINT('',(-51.5061608111161,242.5,85.0000000000015));
#5756=CARTESIAN_POINT('',(-31.5061608111161,242.5,85.0000000000015));
#5757=CARTESIAN_POINT('',(-51.5061608111161,245.5,85.0000000000015));
#5758=CARTESIAN_POINT('Origin',(-51.5061608111161,245.5,77.5000000000015));
#5759=CARTESIAN_POINT('',(-51.5061608111161,245.5,77.5000000000015));
#5760=CARTESIAN_POINT('',(-51.5061608111161,245.5,65.0000000000015));
#5761=CARTESIAN_POINT('',(-51.5061608111161,242.5,77.5000000000015));
#5762=CARTESIAN_POINT('',(-51.5061608111161,242.5,65.0000000000015));
#5763=CARTESIAN_POINT('',(-51.5061608111161,245.5,77.5000000000015));
#5764=CARTESIAN_POINT('Origin',(-74.5061608111161,245.5,77.5000000000015));
#5765=CARTESIAN_POINT('',(-74.5061608111161,245.5,77.5000000000015));
#5766=CARTESIAN_POINT('',(-74.5061608111161,245.5,77.5000000000015));
#5767=CARTESIAN_POINT('',(-74.5061608111161,242.5,77.5000000000015));
#5768=CARTESIAN_POINT('',(-74.5061608111161,242.5,77.5000000000015));
#5769=CARTESIAN_POINT('',(-74.5061608111161,245.5,77.5000000000015));
#5770=CARTESIAN_POINT('Origin',(-74.5061608111161,245.5,112.500000000001));
#5771=CARTESIAN_POINT('',(-74.5061608111161,245.5,112.500000000001));
#5772=CARTESIAN_POINT('',(-74.5061608111161,245.5,112.500000000001));
#5773=CARTESIAN_POINT('',(-74.5061608111161,242.5,112.500000000001));
#5774=CARTESIAN_POINT('',(-74.5061608111161,242.5,112.500000000001));
#5775=CARTESIAN_POINT('',(-74.5061608111161,245.5,112.500000000001));
#5776=CARTESIAN_POINT('Origin',(-24.5061608111161,245.5,112.500000000001));
#5777=CARTESIAN_POINT('',(-24.5061608111161,245.5,112.500000000001));
#5778=CARTESIAN_POINT('',(-24.5061608111161,245.5,112.500000000001));
#5779=CARTESIAN_POINT('',(-24.5061608111161,242.5,112.500000000001));
#5780=CARTESIAN_POINT('',(-24.5061608111161,242.5,112.500000000001));
#5781=CARTESIAN_POINT('',(-24.5061608111161,245.5,112.500000000001));
#5782=CARTESIAN_POINT('Origin',(-24.5061608111161,245.5,77.5000000000015));
#5783=CARTESIAN_POINT('',(-24.5061608111161,245.5,77.5000000000015));
#5784=CARTESIAN_POINT('',(-24.5061608111161,245.5,77.5000000000015));
#5785=CARTESIAN_POINT('',(-24.5061608111161,242.5,77.5000000000015));
#5786=CARTESIAN_POINT('',(-24.5061608111161,242.5,77.5000000000015));
#5787=CARTESIAN_POINT('',(-24.5061608111161,245.5,77.5000000000015));
#5788=CARTESIAN_POINT('Origin',(-31.5061608111161,245.5,77.5000000000015));
#5789=CARTESIAN_POINT('',(-31.5061608111161,245.5,77.5000000000015));
#5790=CARTESIAN_POINT('',(-74.5061608111161,245.5,77.5000000000015));
#5791=CARTESIAN_POINT('',(-31.5061608111161,242.5,77.5000000000015));
#5792=CARTESIAN_POINT('',(-74.5061608111161,242.5,77.5000000000015));
#5793=CARTESIAN_POINT('',(-31.5061608111161,245.5,77.5000000000015));
#5794=CARTESIAN_POINT('Origin',(-31.5061608111161,245.5,105.000000000001));
#5795=CARTESIAN_POINT('',(-31.5061608111161,245.5,85.0000000000015));
#5796=CARTESIAN_POINT('',(-31.5061608111161,242.5,85.0000000000015));
#5797=CARTESIAN_POINT('Origin',(-49.5061608111161,242.5,95.0000000000015));
#5798=CARTESIAN_POINT('Origin',(-49.5061608111161,245.5,95.0000000000015));
#6079=UNCERTAINTY_MEASURE_WITH_UNIT(LENGTH_MEASURE(0.01),#6097,
'DISTANCE_ACCURACY_VALUE',
'Maximum model space distance between geometric entities at asserted c
onnectivities');
#6083=UNCERTAINTY_MEASURE_WITH_UNIT(LENGTH_MEASURE(0.01),#6097,
'DISTANCE_ACCURACY_VALUE',
'Maximum model space distance between geometric entities at asserted c
onnectivities');
#6092=(
GEOMETRIC_REPRESENTATION_CONTEXT(3)
GLOBAL_UNCERTAINTY_ASSIGNED_CONTEXT((#6079))
GLOBAL_UNIT_ASSIGNED_CONTEXT((#6097,#6099,#6100))
REPRESENTATION_CONTEXT('','3D')
);
#6096=(
GEOMETRIC_REPRESENTATION_CONTEXT(3)
GLOBAL_UNCERTAINTY_ASSIGNED_CONTEXT((#6083))
GLOBAL_UNIT_ASSIGNED_CONTEXT((#6097,#6099,#6100))
REPRESENTATION_CONTEXT('','3D')
);
#6097=(
LENGTH_UNIT()
NAMED_UNIT(*)
SI_UNIT(.MILLI.,.METRE.)
);
#6099=(
NAMED_UNIT(*)
PLANE_ANGLE_UNIT()
SI_UNIT($,.RADIAN.)
);
#6100=(
NAMED_UNIT(*)
SI_UNIT($,.STERADIAN.)
SOLID_ANGLE_UNIT()
);
#6109=SHAPE_DEFINITION_REPRESENTATION(#6121,#6144);
#6121=PRODUCT_DEFINITION_SHAPE('',$,#6157);
#6144=SHAPE_REPRESENTATION('',(#3932),#6092);
#6148=PRODUCT_DEFINITION_CONTEXT('part definition',#6186,'design');
#6157=PRODUCT_DEFINITION('Bracket_01','Bracket_01',#6169,#6148);
#6169=PRODUCT_DEFINITION_FORMATION('',$,#6196);
#6186=APPLICATION_CONTEXT(
'Core Data for Automotive Mechanical Design Process');
#6187=PRODUCT_CONTEXT('part definition',#6186,'mechanical');
#6196=PRODUCT('Bracket_01','Bracket_01',$,(#6187));
#6228=COLOUR_RGB('Dark Blue',0.08,0.2,0.34);
#6229=FILL_AREA_STYLE_COLOUR('',#6228);
#6230=FILL_AREA_STYLE('',(#6229));
#6231=SURFACE_STYLE_FILL_AREA(#6230);
#6232=SURFACE_SIDE_STYLE('',(#6231));
#6233=SURFACE_STYLE_USAGE(.BOTH.,#6232);
#6234=PRESENTATION_STYLE_ASSIGNMENT((#6233));
ENDSEC;
END-ISO-10303-21;
